ISO-10303-21;
HEADER;
/* Generated by software containing ST-Developer
 * from STEP Tools, Inc. (www.steptools.com) 
 */

FILE_DESCRIPTION(
/* description */ ('Counterbalanced vertical column'),
/* implementation_level */ '2;1');

FILE_NAME(
/* name */ 'M4 top nut (1).step',
/* time_stamp */ '2026-10-29T16:47:22-07:00',
/* author */ (''),
/* organization */ (''),
/* preprocessor_version */ 'ST-DEVELOPER v20.2',
/* originating_system */ 'Autodesk Translation Framework v15.17.0.0',
/* authorisation */ '');

FILE_SCHEMA (('AUTOMOTIVE_DESIGN { 1 0 10303 214 3 1 1 }'));
ENDSEC;

DATA;
#10=MECHANICAL_DESIGN_GEOMETRIC_PRESENTATION_REPRESENTATION('',(#363),#15040);
#293=SHAPE_REPRESENTATION_RELATIONSHIP('SRR','None',#15197,#328);
#328=ADVANCED_BREP_SHAPE_REPRESENTATION('',(#398),#15016);
#363=STYLED_ITEM('',(#15464),#398);
#398=MANIFOLD_SOLID_BREP('Body1',#7086);
#466=FACE_BOUND('',#1391,.T.);
#467=FACE_BOUND('',#1393,.T.);
#601=PLANE('',#7701);
#602=PLANE('',#7702);
#933=FACE_OUTER_BOUND('',#1388,.T.);
#934=FACE_OUTER_BOUND('',#1389,.T.);
#935=FACE_OUTER_BOUND('',#1390,.T.);
#936=FACE_OUTER_BOUND('',#1392,.T.);
#1388=EDGE_LOOP('',(#5202,#5203,#5204,#5205));
#1389=EDGE_LOOP('',(#5206,#5207,#5208,#5209));
#1390=EDGE_LOOP('',(#5210));
#1391=EDGE_LOOP('',(#5211));
#1392=EDGE_LOOP('',(#5212));
#1393=EDGE_LOOP('',(#5213));
#1884=LINE('',#10810,#2555);
#1885=LINE('',#10816,#2556);
#2555=VECTOR('',#8752,0.165);
#2556=VECTOR('',#8759,0.4);
#3167=CIRCLE('',#7696,0.165);
#3168=CIRCLE('',#7697,0.165);
#3169=CIRCLE('',#7699,0.4);
#3170=CIRCLE('',#7700,0.4);
#3444=VERTEX_POINT('',#10807);
#3445=VERTEX_POINT('',#10809);
#3446=VERTEX_POINT('',#10813);
#3447=VERTEX_POINT('',#10815);
#4102=EDGE_CURVE('',#3444,#3444,#3167,.T.);
#4103=EDGE_CURVE('',#3444,#3445,#1884,.T.);
#4104=EDGE_CURVE('',#3445,#3445,#3168,.T.);
#4105=EDGE_CURVE('',#3446,#3446,#3169,.T.);
#4106=EDGE_CURVE('',#3446,#3447,#1885,.T.);
#4107=EDGE_CURVE('',#3447,#3447,#3170,.T.);
#5202=ORIENTED_EDGE('',*,*,#4102,.F.);
#5203=ORIENTED_EDGE('',*,*,#4103,.T.);
#5204=ORIENTED_EDGE('',*,*,#4104,.T.);
#5205=ORIENTED_EDGE('',*,*,#4103,.F.);
#5206=ORIENTED_EDGE('',*,*,#4105,.F.);
#5207=ORIENTED_EDGE('',*,*,#4106,.T.);
#5208=ORIENTED_EDGE('',*,*,#4107,.T.);
#5209=ORIENTED_EDGE('',*,*,#4106,.F.);
#5210=ORIENTED_EDGE('',*,*,#4105,.T.);
#5211=ORIENTED_EDGE('',*,*,#4102,.T.);
#5212=ORIENTED_EDGE('',*,*,#4107,.F.);
#5213=ORIENTED_EDGE('',*,*,#4104,.F.);
#6611=CYLINDRICAL_SURFACE('',#7695,0.165);
#6612=CYLINDRICAL_SURFACE('',#7698,0.4);
#6775=ADVANCED_FACE('',(#933),#6611,.F.);
#6776=ADVANCED_FACE('',(#934),#6612,.T.);
#6777=ADVANCED_FACE('',(#935,#466),#601,.T.);
#6778=ADVANCED_FACE('',(#936,#467),#602,.F.);
#7086=CLOSED_SHELL('',(#6775,#6776,#6777,#6778));
#7694=AXIS2_PLACEMENT_3D('',#10805,#8746,#8747);
#7695=AXIS2_PLACEMENT_3D('',#10806,#8748,#8749);
#7696=AXIS2_PLACEMENT_3D('',#10808,#8750,#8751);
#7697=AXIS2_PLACEMENT_3D('',#10811,#8753,#8754);
#7698=AXIS2_PLACEMENT_3D('',#10812,#8755,#8756);
#7699=AXIS2_PLACEMENT_3D('',#10814,#8757,#8758);
#7700=AXIS2_PLACEMENT_3D('',#10817,#8760,#8761);
#7701=AXIS2_PLACEMENT_3D('',#10818,#8762,#8763);
#7702=AXIS2_PLACEMENT_3D('',#10819,#8764,#8765);
#8746=DIRECTION('axis',(0.,0.,1.));
#8747=DIRECTION('refdir',(1.,0.,0.));
#8748=DIRECTION('center_axis',(0.,0.,1.));
#8749=DIRECTION('ref_axis',(1.,0.,0.));
#8750=DIRECTION('center_axis',(0.,0.,-1.));
#8751=DIRECTION('ref_axis',(1.,0.,0.));
#8752=DIRECTION('',(0.,0.,-1.));
#8753=DIRECTION('center_axis',(0.,0.,-1.));
#8754=DIRECTION('ref_axis',(1.,0.,0.));
#8755=DIRECTION('center_axis',(0.,0.,1.));
#8756=DIRECTION('ref_axis',(1.,0.,0.));
#8757=DIRECTION('center_axis',(0.,0.,1.));
#8758=DIRECTION('ref_axis',(1.,0.,0.));
#8759=DIRECTION('',(0.,0.,-1.));
#8760=DIRECTION('center_axis',(0.,0.,1.));
#8761=DIRECTION('ref_axis',(1.,0.,0.));
#8762=DIRECTION('center_axis',(0.,0.,1.));
#8763=DIRECTION('ref_axis',(1.,0.,0.));
#8764=DIRECTION('center_axis',(0.,0.,1.));
#8765=DIRECTION('ref_axis',(1.,0.,0.));
#10805=CARTESIAN_POINT('',(0.,0.,0.));
#10806=CARTESIAN_POINT('Origin',(-5.2,0.,20.8));
#10807=CARTESIAN_POINT('',(-5.365,-2.02066721859313E-17,21.2));
#10808=CARTESIAN_POINT('Origin',(-5.2,0.,21.2));
#10809=CARTESIAN_POINT('',(-5.365,-2.02066721859313E-17,20.8));
#10810=CARTESIAN_POINT('',(-5.365,-2.02066721859313E-17,20.8));
#10811=CARTESIAN_POINT('Origin',(-5.2,0.,20.8));
#10812=CARTESIAN_POINT('Origin',(-5.2,0.,20.8));
#10813=CARTESIAN_POINT('',(-5.6,-4.89858719658942E-17,21.2));
#10814=CARTESIAN_POINT('Origin',(-5.2,0.,21.2));
#10815=CARTESIAN_POINT('',(-5.6,-4.89858719658942E-17,20.8));
#10816=CARTESIAN_POINT('',(-5.6,-4.89858719658942E-17,20.8));
#10817=CARTESIAN_POINT('Origin',(-5.2,0.,20.8));
#10818=CARTESIAN_POINT('Origin',(-5.2,0.,21.2));
#10819=CARTESIAN_POINT('Origin',(-5.2,0.,20.8));
#14976=UNCERTAINTY_MEASURE_WITH_UNIT(LENGTH_MEASURE(0.001),#15041,
'DISTANCE_ACCURACY_VALUE',
'Maximum model space distance between geometric entities at asserted c
onnectivities');
#15000=UNCERTAINTY_MEASURE_WITH_UNIT(LENGTH_MEASURE(0.001),#15041,
'DISTANCE_ACCURACY_VALUE',
'Maximum model space distance between geometric entities at asserted c
onnectivities');
#15016=(
GEOMETRIC_REPRESENTATION_CONTEXT(3)
GLOBAL_UNCERTAINTY_ASSIGNED_CONTEXT((#14976))
GLOBAL_UNIT_ASSIGNED_CONTEXT((#15041,#15043,#15044))
REPRESENTATION_CONTEXT('','3D')
);
#15040=(
GEOMETRIC_REPRESENTATION_CONTEXT(3)
GLOBAL_UNCERTAINTY_ASSIGNED_CONTEXT((#15000))
GLOBAL_UNIT_ASSIGNED_CONTEXT((#15041,#15043,#15044))
REPRESENTATION_CONTEXT('','3D')
);
#15041=(
LENGTH_UNIT()
NAMED_UNIT(*)
SI_UNIT(.CENTI.,.METRE.)
);
#15043=(
NAMED_UNIT(*)
PLANE_ANGLE_UNIT()
SI_UNIT($,.RADIAN.)
);
#15044=(
NAMED_UNIT(*)
SI_UNIT($,.STERADIAN.)
SOLID_ANGLE_UNIT()
);
#15060=SHAPE_DEFINITION_REPRESENTATION(#15099,#15197);
#15099=PRODUCT_DEFINITION_SHAPE('',$,#15237);
#15197=SHAPE_REPRESENTATION('',(#7694),#15016);
#15221=PRODUCT_DEFINITION_CONTEXT('part definition',#15340,'design');
#15237=PRODUCT_DEFINITION('M4 top nut (1)','M4 top nut (1)',#15276,#15221);
#15276=PRODUCT_DEFINITION_FORMATION('',$,#15357);
#15340=APPLICATION_CONTEXT(
'Core Data for Automotive Mechanical Design Process');
#15341=PRODUCT_CONTEXT('part definition',#15340,'mechanical');
#15357=PRODUCT('M4 top nut (1)','M4 top nut (1)','M4 top nut (1)',(#15341));
#15458=COLOUR_RGB('Black',0.12,0.14,0.17);
#15459=FILL_AREA_STYLE_COLOUR('',#15458);
#15460=FILL_AREA_STYLE('',(#15459));
#15461=SURFACE_STYLE_FILL_AREA(#15460);
#15462=SURFACE_SIDE_STYLE('',(#15461));
#15463=SURFACE_STYLE_USAGE(.BOTH.,#15462);
#15464=PRESENTATION_STYLE_ASSIGNMENT((#15463));
ENDSEC;
END-ISO-10303-21;
